ISO-10303-21;
HEADER;
/* Generated by software containing ST-Developer
 * from STEP Tools, Inc. (www.steptools.com) 
 */

FILE_DESCRIPTION(
/* description */ ('STEP AP214'),
/* implementation_level */ '2;1');

FILE_NAME(
/* name */ 'Axle Nut.step',
/* time_stamp */ '2026-11-14T06:16:09-08:00',
/* author */ (''),
/* organization */ (''),
/* preprocessor_version */ 'ST-DEVELOPER v20.2',
/* originating_system */ 'Autodesk Translation Framework v15.17.0.0',
/* authorisation */ '');

FILE_SCHEMA (('AUTOMOTIVE_DESIGN { 1 0 10303 214 3 1 1 }'));
ENDSEC;

DATA;
#10=MECHANICAL_DESIGN_GEOMETRIC_PRESENTATION_REPRESENTATION('',(#356),#18006);
#107=(
BOUNDED_CURVE()
B_SPLINE_CURVE(2,(#17477,#17478,#17479),.UNSPECIFIED.,.F.,.F.)
B_SPLINE_CURVE_WITH_KNOTS((3,3),(-2.24923400345372,-1.47749762858512),
 .UNSPECIFIED.)
CURVE()
GEOMETRIC_REPRESENTATION_ITEM()
RATIONAL_B_SPLINE_CURVE((2.5632386809031,2.5632386809031,2.37920642358137))
REPRESENTATION_ITEM('')
);
#108=(
BOUNDED_CURVE()
B_SPLINE_CURVE(2,(#17481,#17482,#17483),.UNSPECIFIED.,.F.,.F.)
B_SPLINE_CURVE_WITH_KNOTS((3,3),(-3.02097037832232,-2.24923400345372),
 .UNSPECIFIED.)
CURVE()
GEOMETRIC_REPRESENTATION_ITEM()
RATIONAL_B_SPLINE_CURVE((2.37920642358137,2.5632386809031,2.5632386809031))
REPRESENTATION_ITEM('')
);
#109=(
BOUNDED_CURVE()
B_SPLINE_CURVE(2,(#17497,#17498,#17499),.UNSPECIFIED.,.F.,.F.)
B_SPLINE_CURVE_WITH_KNOTS((3,3),(-2.24923400345372,-1.47749762858512),
 .UNSPECIFIED.)
CURVE()
GEOMETRIC_REPRESENTATION_ITEM()
RATIONAL_B_SPLINE_CURVE((2.5632386809031,2.5632386809031,2.37920642358137))
REPRESENTATION_ITEM('')
);
#110=(
BOUNDED_CURVE()
B_SPLINE_CURVE(2,(#17500,#17501,#17502),.UNSPECIFIED.,.F.,.F.)
B_SPLINE_CURVE_WITH_KNOTS((3,3),(-3.02097037832232,-2.24923400345372),
 .UNSPECIFIED.)
CURVE()
GEOMETRIC_REPRESENTATION_ITEM()
RATIONAL_B_SPLINE_CURVE((2.37920642358137,2.5632386809031,2.5632386809031))
REPRESENTATION_ITEM('')
);
#111=(
BOUNDED_CURVE()
B_SPLINE_CURVE(2,(#17505,#17506,#17507),.UNSPECIFIED.,.F.,.F.)
B_SPLINE_CURVE_WITH_KNOTS((3,3),(-2.24923400345372,-1.47749762858512),
 .UNSPECIFIED.)
CURVE()
GEOMETRIC_REPRESENTATION_ITEM()
RATIONAL_B_SPLINE_CURVE((2.5632386809031,2.5632386809031,2.37920642358137))
REPRESENTATION_ITEM('')
);
#112=(
BOUNDED_CURVE()
B_SPLINE_CURVE(2,(#17508,#17509,#17510),.UNSPECIFIED.,.F.,.F.)
B_SPLINE_CURVE_WITH_KNOTS((3,3),(-3.02097037832232,-2.24923400345372),
 .UNSPECIFIED.)
CURVE()
GEOMETRIC_REPRESENTATION_ITEM()
RATIONAL_B_SPLINE_CURVE((2.37920642358137,2.5632386809031,2.5632386809031))
REPRESENTATION_ITEM('')
);
#113=(
BOUNDED_CURVE()
B_SPLINE_CURVE(2,(#17513,#17514,#17515),.UNSPECIFIED.,.F.,.F.)
B_SPLINE_CURVE_WITH_KNOTS((3,3),(-2.24923400345372,-1.47749762858512),
 .UNSPECIFIED.)
CURVE()
GEOMETRIC_REPRESENTATION_ITEM()
RATIONAL_B_SPLINE_CURVE((2.5632386809031,2.5632386809031,2.37920642358137))
REPRESENTATION_ITEM('')
);
#114=(
BOUNDED_CURVE()
B_SPLINE_CURVE(2,(#17516,#17517,#17518),.UNSPECIFIED.,.F.,.F.)
B_SPLINE_CURVE_WITH_KNOTS((3,3),(-3.02097037832232,-2.24923400345372),
 .UNSPECIFIED.)
CURVE()
GEOMETRIC_REPRESENTATION_ITEM()
RATIONAL_B_SPLINE_CURVE((2.37920642358137,2.5632386809031,2.5632386809031))
REPRESENTATION_ITEM('')
);
#115=(
BOUNDED_CURVE()
B_SPLINE_CURVE(2,(#17521,#17522,#17523),.UNSPECIFIED.,.F.,.F.)
B_SPLINE_CURVE_WITH_KNOTS((3,3),(-2.24923400345372,-1.47749762858512),
 .UNSPECIFIED.)
CURVE()
GEOMETRIC_REPRESENTATION_ITEM()
RATIONAL_B_SPLINE_CURVE((2.5632386809031,2.5632386809031,2.37920642358137))
REPRESENTATION_ITEM('')
);
#116=(
BOUNDED_CURVE()
B_SPLINE_CURVE(2,(#17524,#17525,#17526),.UNSPECIFIED.,.F.,.F.)
B_SPLINE_CURVE_WITH_KNOTS((3,3),(-3.02097037832232,-2.24923400345372),
 .UNSPECIFIED.)
CURVE()
GEOMETRIC_REPRESENTATION_ITEM()
RATIONAL_B_SPLINE_CURVE((2.37920642358137,2.5632386809031,2.5632386809031))
REPRESENTATION_ITEM('')
);
#117=(
BOUNDED_CURVE()
B_SPLINE_CURVE(2,(#17529,#17530,#17531),.UNSPECIFIED.,.F.,.F.)
B_SPLINE_CURVE_WITH_KNOTS((3,3),(-2.24923400345372,-1.47749762858512),
 .UNSPECIFIED.)
CURVE()
GEOMETRIC_REPRESENTATION_ITEM()
RATIONAL_B_SPLINE_CURVE((2.5632386809031,2.5632386809031,2.37920642358137))
REPRESENTATION_ITEM('')
);
#118=(
BOUNDED_CURVE()
B_SPLINE_CURVE(2,(#17532,#17533,#17534),.UNSPECIFIED.,.F.,.F.)
B_SPLINE_CURVE_WITH_KNOTS((3,3),(-3.02097037832232,-2.24923400345372),
 .UNSPECIFIED.)
CURVE()
GEOMETRIC_REPRESENTATION_ITEM()
RATIONAL_B_SPLINE_CURVE((2.37920642358137,2.5632386809031,2.5632386809031))
REPRESENTATION_ITEM('')
);
#129=CONICAL_SURFACE('',#10601,3.175,0.785398163397448);
#130=CONICAL_SURFACE('',#10607,2.48793,0.785398163397449);
#131=CONICAL_SURFACE('',#10609,5.4991,1.30899693899575);
#132=CONICAL_SURFACE('',#10617,5.4991,1.30899693899575);
#133=CONICAL_SURFACE('',#10618,5.4991,1.30899693899575);
#134=CONICAL_SURFACE('',#10619,5.4991,1.30899693899575);
#135=CONICAL_SURFACE('',#10620,5.4991,1.30899693899575);
#136=CONICAL_SURFACE('',#10621,5.4991,1.30899693899575);
#324=SHAPE_REPRESENTATION_RELATIONSHIP('SRR','None',#18082,#340);
#340=ADVANCED_BREP_SHAPE_REPRESENTATION('',(#372),#17999);
#356=STYLED_ITEM('',(#18172),#372);
#372=MANIFOLD_SOLID_BREP('Body1',#9565);
#476=FACE_BOUND('',#1983,.T.);
#477=FACE_BOUND('',#1996,.T.);
#791=PLANE('',#10611);
#792=PLANE('',#10622);
#793=PLANE('',#10623);
#794=PLANE('',#10624);
#795=PLANE('',#10625);
#796=PLANE('',#10626);
#797=PLANE('',#10627);
#798=PLANE('',#10628);
#799=PLANE('',#10629);
#800=PLANE('',#10630);
#801=PLANE('',#10631);
#802=PLANE('',#10632);
#803=PLANE('',#10633);
#804=PLANE('',#10634);
#1304=FACE_OUTER_BOUND('',#1977,.T.);
#1305=FACE_OUTER_BOUND('',#1978,.T.);
#1306=FACE_OUTER_BOUND('',#1979,.T.);
#1307=FACE_OUTER_BOUND('',#1980,.T.);
#1308=FACE_OUTER_BOUND('',#1981,.T.);
#1309=FACE_OUTER_BOUND('',#1982,.T.);
#1310=FACE_OUTER_BOUND('',#1984,.T.);
#1311=FACE_OUTER_BOUND('',#1985,.T.);
#1312=FACE_OUTER_BOUND('',#1986,.T.);
#1313=FACE_OUTER_BOUND('',#1987,.T.);
#1314=FACE_OUTER_BOUND('',#1988,.T.);
#1315=FACE_OUTER_BOUND('',#1989,.T.);
#1316=FACE_OUTER_BOUND('',#1990,.T.);
#1317=FACE_OUTER_BOUND('',#1991,.T.);
#1318=FACE_OUTER_BOUND('',#1992,.T.);
#1319=FACE_OUTER_BOUND('',#1993,.T.);
#1320=FACE_OUTER_BOUND('',#1994,.T.);
#1321=FACE_OUTER_BOUND('',#1995,.T.);
#1322=FACE_OUTER_BOUND('',#1997,.T.);
#1323=FACE_OUTER_BOUND('',#1998,.T.);
#1324=FACE_OUTER_BOUND('',#1999,.T.);
#1325=FACE_OUTER_BOUND('',#2000,.T.);
#1326=FACE_OUTER_BOUND('',#2001,.T.);
#1327=FACE_OUTER_BOUND('',#2002,.T.);
#1977=EDGE_LOOP('',(#8362,#8363,#8364,#8365,#8366,#8367,#8368,#8369,#8370));
#1978=EDGE_LOOP('',(#8371,#8372,#8373,#8374,#8375));
#1979=EDGE_LOOP('',(#8376,#8377,#8378,#8379,#8380));
#1980=EDGE_LOOP('',(#8381,#8382,#8383,#8384));
#1981=EDGE_LOOP('',(#8385,#8386,#8387));
#1982=EDGE_LOOP('',(#8388,#8389,#8390,#8391,#8392,#8393));
#1983=EDGE_LOOP('',(#8394));
#1984=EDGE_LOOP('',(#8395,#8396,#8397));
#1985=EDGE_LOOP('',(#8398,#8399,#8400));
#1986=EDGE_LOOP('',(#8401,#8402,#8403));
#1987=EDGE_LOOP('',(#8404,#8405,#8406));
#1988=EDGE_LOOP('',(#8407,#8408,#8409));
#1989=EDGE_LOOP('',(#8410,#8411,#8412,#8413,#8414,#8415));
#1990=EDGE_LOOP('',(#8416,#8417,#8418,#8419,#8420,#8421));
#1991=EDGE_LOOP('',(#8422,#8423,#8424,#8425,#8426,#8427));
#1992=EDGE_LOOP('',(#8428,#8429,#8430,#8431,#8432,#8433));
#1993=EDGE_LOOP('',(#8434,#8435,#8436,#8437,#8438,#8439));
#1994=EDGE_LOOP('',(#8440,#8441,#8442,#8443,#8444,#8445));
#1995=EDGE_LOOP('',(#8446));
#1996=EDGE_LOOP('',(#8447));
#1997=EDGE_LOOP('',(#8448,#8449,#8450));
#1998=EDGE_LOOP('',(#8451,#8452,#8453));
#1999=EDGE_LOOP('',(#8454,#8455,#8456));
#2000=EDGE_LOOP('',(#8457,#8458,#8459));
#2001=EDGE_LOOP('',(#8460,#8461,#8462));
#2002=EDGE_LOOP('',(#8463,#8464,#8465));
#2757=LINE('',#17446,#3481);
#2758=LINE('',#17463,#3482);
#2759=LINE('',#17468,#3483);
#2760=LINE('',#17472,#3484);
#2761=LINE('',#17537,#3485);
#2762=LINE('',#17538,#3486);
#2763=LINE('',#17540,#3487);
#2764=LINE('',#17541,#3488);
#2765=LINE('',#17544,#3489);
#2766=LINE('',#17545,#3490);
#2767=LINE('',#17546,#3491);
#2768=LINE('',#17549,#3492);
#2769=LINE('',#17550,#3493);
#2770=LINE('',#17551,#3494);
#2771=LINE('',#17554,#3495);
#2772=LINE('',#17555,#3496);
#2773=LINE('',#17556,#3497);
#2774=LINE('',#17559,#3498);
#2775=LINE('',#17560,#3499);
#2776=LINE('',#17561,#3500);
#2777=LINE('',#17563,#3501);
#2778=LINE('',#17564,#3502);
#3481=VECTOR('',#13194,5.4991);
#3482=VECTOR('',#13211,3.175);
#3483=VECTOR('',#13218,2.48793);
#3484=VECTOR('',#13223,2.48793);
#3485=VECTOR('',#13254,1000.);
#3486=VECTOR('',#13255,1000.);
#3487=VECTOR('',#13256,1000.);
#3488=VECTOR('',#13257,1000.);
#3489=VECTOR('',#13260,1000.);
#3490=VECTOR('',#13261,1000.);
#3491=VECTOR('',#13262,1000.);
#3492=VECTOR('',#13265,1000.);
#3493=VECTOR('',#13266,1000.);
#3494=VECTOR('',#13267,1000.);
#3495=VECTOR('',#13270,1000.);
#3496=VECTOR('',#13271,1000.);
#3497=VECTOR('',#13272,1000.);
#3498=VECTOR('',#13275,1000.);
#3499=VECTOR('',#13276,1000.);
#3500=VECTOR('',#13277,1000.);
#3501=VECTOR('',#13280,1000.);
#3502=VECTOR('',#13281,1000.);
#3885=CIRCLE('',#10594,5.4991);
#3886=CIRCLE('',#10595,5.4991);
#3887=CIRCLE('',#10596,5.4991);
#3888=CIRCLE('',#10597,5.4991);
#3889=CIRCLE('',#10598,5.4991);
#3890=CIRCLE('',#10599,5.4991);
#3891=CIRCLE('',#10600,5.4991);
#3892=CIRCLE('',#10602,2.48793);
#3893=CIRCLE('',#10603,3.175);
#3894=CIRCLE('',#10604,2.48793);
#3895=CIRCLE('',#10606,2.48793);
#3896=CIRCLE('',#10608,3.175);
#3897=CIRCLE('',#10610,5.4991);
#3898=CIRCLE('',#10612,5.4991);
#3899=CIRCLE('',#10613,5.4991);
#3900=CIRCLE('',#10614,5.4991);
#3901=CIRCLE('',#10615,5.4991);
#3902=CIRCLE('',#10616,5.4991);
#4686=VERTEX_POINT('',#17443);
#4687=VERTEX_POINT('',#17445);
#4688=VERTEX_POINT('',#17447);
#4689=VERTEX_POINT('',#17449);
#4690=VERTEX_POINT('',#17451);
#4691=VERTEX_POINT('',#17453);
#4692=VERTEX_POINT('',#17455);
#4693=VERTEX_POINT('',#17459);
#4694=VERTEX_POINT('',#17460);
#4695=VERTEX_POINT('',#17462);
#4696=VERTEX_POINT('',#17467);
#4697=VERTEX_POINT('',#17471);
#4698=VERTEX_POINT('',#17475);
#4699=VERTEX_POINT('',#17476);
#4700=VERTEX_POINT('',#17480);
#4701=VERTEX_POINT('',#17486);
#4702=VERTEX_POINT('',#17487);
#4703=VERTEX_POINT('',#17489);
#4704=VERTEX_POINT('',#17492);
#4705=VERTEX_POINT('',#17496);
#4706=VERTEX_POINT('',#17504);
#4707=VERTEX_POINT('',#17512);
#4708=VERTEX_POINT('',#17520);
#4709=VERTEX_POINT('',#17528);
#4710=VERTEX_POINT('',#17536);
#4711=VERTEX_POINT('',#17539);
#4712=VERTEX_POINT('',#17543);
#4713=VERTEX_POINT('',#17548);
#4714=VERTEX_POINT('',#17553);
#4715=VERTEX_POINT('',#17558);
#5929=EDGE_CURVE('',#4686,#4686,#3885,.T.);
#5930=EDGE_CURVE('',#4686,#4687,#2757,.T.);
#5931=EDGE_CURVE('',#4687,#4688,#3886,.T.);
#5932=EDGE_CURVE('',#4688,#4689,#3887,.T.);
#5933=EDGE_CURVE('',#4689,#4690,#3888,.T.);
#5934=EDGE_CURVE('',#4690,#4691,#3889,.T.);
#5935=EDGE_CURVE('',#4691,#4692,#3890,.T.);
#5936=EDGE_CURVE('',#4692,#4687,#3891,.T.);
#5937=EDGE_CURVE('',#4693,#4694,#3892,.T.);
#5938=EDGE_CURVE('',#4694,#4695,#2758,.T.);
#5939=EDGE_CURVE('',#4695,#4695,#3893,.T.);
#5940=EDGE_CURVE('',#4694,#4693,#3894,.T.);
#5941=EDGE_CURVE('',#4693,#4696,#2759,.T.);
#5942=EDGE_CURVE('',#4696,#4696,#3895,.T.);
#5943=EDGE_CURVE('',#4696,#4697,#2760,.T.);
#5944=EDGE_CURVE('',#4697,#4697,#3896,.T.);
#5945=EDGE_CURVE('',#4698,#4699,#107,.T.);
#5946=EDGE_CURVE('',#4699,#4700,#108,.T.);
#5947=EDGE_CURVE('',#4700,#4698,#3897,.T.);
#5948=EDGE_CURVE('',#4701,#4702,#3898,.T.);
#5949=EDGE_CURVE('',#4703,#4701,#3899,.T.);
#5950=EDGE_CURVE('',#4698,#4703,#3900,.T.);
#5951=EDGE_CURVE('',#4704,#4700,#3901,.T.);
#5952=EDGE_CURVE('',#4702,#4704,#3902,.T.);
#5953=EDGE_CURVE('',#4702,#4705,#109,.T.);
#5954=EDGE_CURVE('',#4705,#4701,#110,.T.);
#5955=EDGE_CURVE('',#4701,#4706,#111,.T.);
#5956=EDGE_CURVE('',#4706,#4703,#112,.T.);
#5957=EDGE_CURVE('',#4703,#4707,#113,.T.);
#5958=EDGE_CURVE('',#4707,#4698,#114,.T.);
#5959=EDGE_CURVE('',#4700,#4708,#115,.T.);
#5960=EDGE_CURVE('',#4708,#4704,#116,.T.);
#5961=EDGE_CURVE('',#4704,#4709,#117,.T.);
#5962=EDGE_CURVE('',#4709,#4702,#118,.T.);
#5963=EDGE_CURVE('',#4710,#4707,#2761,.T.);
#5964=EDGE_CURVE('',#4688,#4710,#2762,.T.);
#5965=EDGE_CURVE('',#4711,#4688,#2763,.T.);
#5966=EDGE_CURVE('',#4711,#4699,#2764,.T.);
#5967=EDGE_CURVE('',#4712,#4706,#2765,.T.);
#5968=EDGE_CURVE('',#4689,#4712,#2766,.T.);
#5969=EDGE_CURVE('',#4710,#4689,#2767,.T.);
#5970=EDGE_CURVE('',#4713,#4705,#2768,.T.);
#5971=EDGE_CURVE('',#4690,#4713,#2769,.T.);
#5972=EDGE_CURVE('',#4712,#4690,#2770,.T.);
#5973=EDGE_CURVE('',#4714,#4709,#2771,.T.);
#5974=EDGE_CURVE('',#4691,#4714,#2772,.T.);
#5975=EDGE_CURVE('',#4713,#4691,#2773,.T.);
#5976=EDGE_CURVE('',#4715,#4708,#2774,.T.);
#5977=EDGE_CURVE('',#4692,#4715,#2775,.T.);
#5978=EDGE_CURVE('',#4714,#4692,#2776,.T.);
#5979=EDGE_CURVE('',#4687,#4711,#2777,.T.);
#5980=EDGE_CURVE('',#4715,#4687,#2778,.T.);
#8362=ORIENTED_EDGE('',*,*,#5929,.F.);
#8363=ORIENTED_EDGE('',*,*,#5930,.T.);
#8364=ORIENTED_EDGE('',*,*,#5931,.T.);
#8365=ORIENTED_EDGE('',*,*,#5932,.T.);
#8366=ORIENTED_EDGE('',*,*,#5933,.T.);
#8367=ORIENTED_EDGE('',*,*,#5934,.T.);
#8368=ORIENTED_EDGE('',*,*,#5935,.T.);
#8369=ORIENTED_EDGE('',*,*,#5936,.T.);
#8370=ORIENTED_EDGE('',*,*,#5930,.F.);
#8371=ORIENTED_EDGE('',*,*,#5937,.T.);
#8372=ORIENTED_EDGE('',*,*,#5938,.T.);
#8373=ORIENTED_EDGE('',*,*,#5939,.F.);
#8374=ORIENTED_EDGE('',*,*,#5938,.F.);
#8375=ORIENTED_EDGE('',*,*,#5940,.T.);
#8376=ORIENTED_EDGE('',*,*,#5937,.F.);
#8377=ORIENTED_EDGE('',*,*,#5941,.T.);
#8378=ORIENTED_EDGE('',*,*,#5942,.T.);
#8379=ORIENTED_EDGE('',*,*,#5941,.F.);
#8380=ORIENTED_EDGE('',*,*,#5940,.F.);
#8381=ORIENTED_EDGE('',*,*,#5942,.F.);
#8382=ORIENTED_EDGE('',*,*,#5943,.T.);
#8383=ORIENTED_EDGE('',*,*,#5944,.T.);
#8384=ORIENTED_EDGE('',*,*,#5943,.F.);
#8385=ORIENTED_EDGE('',*,*,#5945,.T.);
#8386=ORIENTED_EDGE('',*,*,#5946,.T.);
#8387=ORIENTED_EDGE('',*,*,#5947,.T.);
#8388=ORIENTED_EDGE('',*,*,#5948,.F.);
#8389=ORIENTED_EDGE('',*,*,#5949,.F.);
#8390=ORIENTED_EDGE('',*,*,#5950,.F.);
#8391=ORIENTED_EDGE('',*,*,#5947,.F.);
#8392=ORIENTED_EDGE('',*,*,#5951,.F.);
#8393=ORIENTED_EDGE('',*,*,#5952,.F.);
#8394=ORIENTED_EDGE('',*,*,#5939,.T.);
#8395=ORIENTED_EDGE('',*,*,#5948,.T.);
#8396=ORIENTED_EDGE('',*,*,#5953,.T.);
#8397=ORIENTED_EDGE('',*,*,#5954,.T.);
#8398=ORIENTED_EDGE('',*,*,#5949,.T.);
#8399=ORIENTED_EDGE('',*,*,#5955,.T.);
#8400=ORIENTED_EDGE('',*,*,#5956,.T.);
#8401=ORIENTED_EDGE('',*,*,#5950,.T.);
#8402=ORIENTED_EDGE('',*,*,#5957,.T.);
#8403=ORIENTED_EDGE('',*,*,#5958,.T.);
#8404=ORIENTED_EDGE('',*,*,#5951,.T.);
#8405=ORIENTED_EDGE('',*,*,#5959,.T.);
#8406=ORIENTED_EDGE('',*,*,#5960,.T.);
#8407=ORIENTED_EDGE('',*,*,#5952,.T.);
#8408=ORIENTED_EDGE('',*,*,#5961,.T.);
#8409=ORIENTED_EDGE('',*,*,#5962,.T.);
#8410=ORIENTED_EDGE('',*,*,#5963,.F.);
#8411=ORIENTED_EDGE('',*,*,#5964,.F.);
#8412=ORIENTED_EDGE('',*,*,#5965,.F.);
#8413=ORIENTED_EDGE('',*,*,#5966,.T.);
#8414=ORIENTED_EDGE('',*,*,#5945,.F.);
#8415=ORIENTED_EDGE('',*,*,#5958,.F.);
#8416=ORIENTED_EDGE('',*,*,#5967,.F.);
#8417=ORIENTED_EDGE('',*,*,#5968,.F.);
#8418=ORIENTED_EDGE('',*,*,#5969,.F.);
#8419=ORIENTED_EDGE('',*,*,#5963,.T.);
#8420=ORIENTED_EDGE('',*,*,#5957,.F.);
#8421=ORIENTED_EDGE('',*,*,#5956,.F.);
#8422=ORIENTED_EDGE('',*,*,#5970,.F.);
#8423=ORIENTED_EDGE('',*,*,#5971,.F.);
#8424=ORIENTED_EDGE('',*,*,#5972,.F.);
#8425=ORIENTED_EDGE('',*,*,#5967,.T.);
#8426=ORIENTED_EDGE('',*,*,#5955,.F.);
#8427=ORIENTED_EDGE('',*,*,#5954,.F.);
#8428=ORIENTED_EDGE('',*,*,#5973,.F.);
#8429=ORIENTED_EDGE('',*,*,#5974,.F.);
#8430=ORIENTED_EDGE('',*,*,#5975,.F.);
#8431=ORIENTED_EDGE('',*,*,#5970,.T.);
#8432=ORIENTED_EDGE('',*,*,#5953,.F.);
#8433=ORIENTED_EDGE('',*,*,#5962,.F.);
#8434=ORIENTED_EDGE('',*,*,#5976,.F.);
#8435=ORIENTED_EDGE('',*,*,#5977,.F.);
#8436=ORIENTED_EDGE('',*,*,#5978,.F.);
#8437=ORIENTED_EDGE('',*,*,#5973,.T.);
#8438=ORIENTED_EDGE('',*,*,#5961,.F.);
#8439=ORIENTED_EDGE('',*,*,#5960,.F.);
#8440=ORIENTED_EDGE('',*,*,#5966,.F.);
#8441=ORIENTED_EDGE('',*,*,#5979,.F.);
#8442=ORIENTED_EDGE('',*,*,#5980,.F.);
#8443=ORIENTED_EDGE('',*,*,#5976,.T.);
#8444=ORIENTED_EDGE('',*,*,#5959,.F.);
#8445=ORIENTED_EDGE('',*,*,#5946,.F.);
#8446=ORIENTED_EDGE('',*,*,#5929,.T.);
#8447=ORIENTED_EDGE('',*,*,#5944,.F.);
#8448=ORIENTED_EDGE('',*,*,#5964,.T.);
#8449=ORIENTED_EDGE('',*,*,#5969,.T.);
#8450=ORIENTED_EDGE('',*,*,#5932,.F.);
#8451=ORIENTED_EDGE('',*,*,#5931,.F.);
#8452=ORIENTED_EDGE('',*,*,#5979,.T.);
#8453=ORIENTED_EDGE('',*,*,#5965,.T.);
#8454=ORIENTED_EDGE('',*,*,#5968,.T.);
#8455=ORIENTED_EDGE('',*,*,#5972,.T.);
#8456=ORIENTED_EDGE('',*,*,#5933,.F.);
#8457=ORIENTED_EDGE('',*,*,#5936,.F.);
#8458=ORIENTED_EDGE('',*,*,#5977,.T.);
#8459=ORIENTED_EDGE('',*,*,#5980,.T.);
#8460=ORIENTED_EDGE('',*,*,#5935,.F.);
#8461=ORIENTED_EDGE('',*,*,#5974,.T.);
#8462=ORIENTED_EDGE('',*,*,#5978,.T.);
#8463=ORIENTED_EDGE('',*,*,#5971,.T.);
#8464=ORIENTED_EDGE('',*,*,#5975,.T.);
#8465=ORIENTED_EDGE('',*,*,#5934,.F.);
#8961=CYLINDRICAL_SURFACE('',#10593,5.4991);
#8962=CYLINDRICAL_SURFACE('',#10605,2.48793);
#9443=ADVANCED_FACE('',(#1304),#8961,.T.);
#9444=ADVANCED_FACE('',(#1305),#129,.F.);
#9445=ADVANCED_FACE('',(#1306),#8962,.F.);
#9446=ADVANCED_FACE('',(#1307),#130,.F.);
#9447=ADVANCED_FACE('',(#1308),#131,.T.);
#9448=ADVANCED_FACE('',(#1309,#476),#791,.F.);
#9449=ADVANCED_FACE('',(#1310),#132,.T.);
#9450=ADVANCED_FACE('',(#1311),#133,.T.);
#9451=ADVANCED_FACE('',(#1312),#134,.T.);
#9452=ADVANCED_FACE('',(#1313),#135,.T.);
#9453=ADVANCED_FACE('',(#1314),#136,.T.);
#9454=ADVANCED_FACE('',(#1315),#792,.F.);
#9455=ADVANCED_FACE('',(#1316),#793,.F.);
#9456=ADVANCED_FACE('',(#1317),#794,.F.);
#9457=ADVANCED_FACE('',(#1318),#795,.F.);
#9458=ADVANCED_FACE('',(#1319),#796,.F.);
#9459=ADVANCED_FACE('',(#1320),#797,.F.);
#9460=ADVANCED_FACE('',(#1321,#477),#798,.F.);
#9461=ADVANCED_FACE('',(#1322),#799,.F.);
#9462=ADVANCED_FACE('',(#1323),#800,.F.);
#9463=ADVANCED_FACE('',(#1324),#801,.F.);
#9464=ADVANCED_FACE('',(#1325),#802,.F.);
#9465=ADVANCED_FACE('',(#1326),#803,.F.);
#9466=ADVANCED_FACE('',(#1327),#804,.F.);
#9565=CLOSED_SHELL('',(#9443,#9444,#9445,#9446,#9447,#9448,#9449,#9450,
#9451,#9452,#9453,#9454,#9455,#9456,#9457,#9458,#9459,#9460,#9461,#9462,
#9463,#9464,#9465,#9466));
#10592=AXIS2_PLACEMENT_3D('',#17441,#13188,#13189);
#10593=AXIS2_PLACEMENT_3D('',#17442,#13190,#13191);
#10594=AXIS2_PLACEMENT_3D('',#17444,#13192,#13193);
#10595=AXIS2_PLACEMENT_3D('',#17448,#13195,#13196);
#10596=AXIS2_PLACEMENT_3D('',#17450,#13197,#13198);
#10597=AXIS2_PLACEMENT_3D('',#17452,#13199,#13200);
#10598=AXIS2_PLACEMENT_3D('',#17454,#13201,#13202);
#10599=AXIS2_PLACEMENT_3D('',#17456,#13203,#13204);
#10600=AXIS2_PLACEMENT_3D('',#17457,#13205,#13206);
#10601=AXIS2_PLACEMENT_3D('',#17458,#13207,#13208);
#10602=AXIS2_PLACEMENT_3D('',#17461,#13209,#13210);
#10603=AXIS2_PLACEMENT_3D('',#17464,#13212,#13213);
#10604=AXIS2_PLACEMENT_3D('',#17465,#13214,#13215);
#10605=AXIS2_PLACEMENT_3D('',#17466,#13216,#13217);
#10606=AXIS2_PLACEMENT_3D('',#17469,#13219,#13220);
#10607=AXIS2_PLACEMENT_3D('',#17470,#13221,#13222);
#10608=AXIS2_PLACEMENT_3D('',#17473,#13224,#13225);
#10609=AXIS2_PLACEMENT_3D('',#17474,#13226,#13227);
#10610=AXIS2_PLACEMENT_3D('',#17484,#13228,#13229);
#10611=AXIS2_PLACEMENT_3D('',#17485,#13230,#13231);
#10612=AXIS2_PLACEMENT_3D('',#17488,#13232,#13233);
#10613=AXIS2_PLACEMENT_3D('',#17490,#13234,#13235);
#10614=AXIS2_PLACEMENT_3D('',#17491,#13236,#13237);
#10615=AXIS2_PLACEMENT_3D('',#17493,#13238,#13239);
#10616=AXIS2_PLACEMENT_3D('',#17494,#13240,#13241);
#10617=AXIS2_PLACEMENT_3D('',#17495,#13242,#13243);
#10618=AXIS2_PLACEMENT_3D('',#17503,#13244,#13245);
#10619=AXIS2_PLACEMENT_3D('',#17511,#13246,#13247);
#10620=AXIS2_PLACEMENT_3D('',#17519,#13248,#13249);
#10621=AXIS2_PLACEMENT_3D('',#17527,#13250,#13251);
#10622=AXIS2_PLACEMENT_3D('',#17535,#13252,#13253);
#10623=AXIS2_PLACEMENT_3D('',#17542,#13258,#13259);
#10624=AXIS2_PLACEMENT_3D('',#17547,#13263,#13264);
#10625=AXIS2_PLACEMENT_3D('',#17552,#13268,#13269);
#10626=AXIS2_PLACEMENT_3D('',#17557,#13273,#13274);
#10627=AXIS2_PLACEMENT_3D('',#17562,#13278,#13279);
#10628=AXIS2_PLACEMENT_3D('',#17565,#13282,#13283);
#10629=AXIS2_PLACEMENT_3D('',#17566,#13284,#13285);
#10630=AXIS2_PLACEMENT_3D('',#17567,#13286,#13287);
#10631=AXIS2_PLACEMENT_3D('',#17568,#13288,#13289);
#10632=AXIS2_PLACEMENT_3D('',#17569,#13290,#13291);
#10633=AXIS2_PLACEMENT_3D('',#17570,#13292,#13293);
#10634=AXIS2_PLACEMENT_3D('',#17571,#13294,#13295);
#13188=DIRECTION('axis',(0.,0.,1.));
#13189=DIRECTION('refdir',(1.,0.,0.));
#13190=DIRECTION('center_axis',(1.,0.,0.));
#13191=DIRECTION('ref_axis',(0.,0.,-1.));
#13192=DIRECTION('center_axis',(1.,0.,0.));
#13193=DIRECTION('ref_axis',(0.,0.,-1.));
#13194=DIRECTION('',(-1.,0.,0.));
#13195=DIRECTION('center_axis',(1.,0.,0.));
#13196=DIRECTION('ref_axis',(0.,0.,-1.));
#13197=DIRECTION('center_axis',(1.,0.,0.));
#13198=DIRECTION('ref_axis',(0.,0.,-1.));
#13199=DIRECTION('center_axis',(1.,0.,0.));
#13200=DIRECTION('ref_axis',(0.,0.,-1.));
#13201=DIRECTION('center_axis',(1.,0.,0.));
#13202=DIRECTION('ref_axis',(0.,0.,-1.));
#13203=DIRECTION('center_axis',(1.,0.,0.));
#13204=DIRECTION('ref_axis',(0.,0.,-1.));
#13205=DIRECTION('center_axis',(1.,0.,0.));
#13206=DIRECTION('ref_axis',(0.,0.,-1.));
#13207=DIRECTION('center_axis',(-1.,0.,0.));
#13208=DIRECTION('ref_axis',(0.,0.,1.));
#13209=DIRECTION('center_axis',(1.,0.,0.));
#13210=DIRECTION('ref_axis',(0.,0.,-1.));
#13211=DIRECTION('',(-0.707106781186548,-8.65956056235493E-17,-0.707106781186547));
#13212=DIRECTION('center_axis',(1.,0.,0.));
#13213=DIRECTION('ref_axis',(0.,0.,-1.));
#13214=DIRECTION('center_axis',(1.,0.,0.));
#13215=DIRECTION('ref_axis',(0.,0.,-1.));
#13216=DIRECTION('center_axis',(1.,0.,0.));
#13217=DIRECTION('ref_axis',(0.,0.,-1.));
#13218=DIRECTION('',(1.,0.,0.));
#13219=DIRECTION('center_axis',(1.,0.,0.));
#13220=DIRECTION('ref_axis',(0.,0.,-1.));
#13221=DIRECTION('center_axis',(1.,0.,0.));
#13222=DIRECTION('ref_axis',(0.,0.,-1.));
#13223=DIRECTION('',(0.707106781186547,-8.65956056235494E-17,0.707106781186548));
#13224=DIRECTION('center_axis',(1.,0.,0.));
#13225=DIRECTION('ref_axis',(0.,0.,-1.));
#13226=DIRECTION('center_axis',(1.,0.,0.));
#13227=DIRECTION('ref_axis',(0.,0.,-1.));
#13228=DIRECTION('center_axis',(1.,0.,0.));
#13229=DIRECTION('ref_axis',(0.,0.,-1.));
#13230=DIRECTION('center_axis',(1.,0.,0.));
#13231=DIRECTION('ref_axis',(0.,1.,0.));
#13232=DIRECTION('center_axis',(1.,0.,0.));
#13233=DIRECTION('ref_axis',(0.,0.,-1.));
#13234=DIRECTION('center_axis',(1.,0.,0.));
#13235=DIRECTION('ref_axis',(0.,0.,-1.));
#13236=DIRECTION('center_axis',(1.,0.,0.));
#13237=DIRECTION('ref_axis',(0.,0.,-1.));
#13238=DIRECTION('center_axis',(1.,0.,0.));
#13239=DIRECTION('ref_axis',(0.,0.,-1.));
#13240=DIRECTION('center_axis',(1.,0.,0.));
#13241=DIRECTION('ref_axis',(0.,0.,-1.));
#13242=DIRECTION('center_axis',(1.,0.,0.));
#13243=DIRECTION('ref_axis',(0.,0.,-1.));
#13244=DIRECTION('center_axis',(1.,0.,0.));
#13245=DIRECTION('ref_axis',(0.,0.,-1.));
#13246=DIRECTION('center_axis',(1.,0.,0.));
#13247=DIRECTION('ref_axis',(0.,0.,-1.));
#13248=DIRECTION('center_axis',(1.,0.,0.));
#13249=DIRECTION('ref_axis',(0.,0.,-1.));
#13250=DIRECTION('center_axis',(1.,0.,0.));
#13251=DIRECTION('ref_axis',(0.,0.,-1.));
#13252=DIRECTION('center_axis',(0.,0.866025403784439,-0.5));
#13253=DIRECTION('ref_axis',(-1.,0.,0.));
#13254=DIRECTION('',(-1.,0.,0.));
#13255=DIRECTION('',(0.,-0.5,-0.866025403784439));
#13256=DIRECTION('',(0.,-0.5,-0.866025403784439));
#13257=DIRECTION('',(-1.,0.,0.));
#13258=DIRECTION('center_axis',(0.,0.866025403784439,0.5));
#13259=DIRECTION('ref_axis',(1.,0.,0.));
#13260=DIRECTION('',(-1.,0.,0.));
#13261=DIRECTION('',(0.,0.5,-0.866025403784439));
#13262=DIRECTION('',(0.,0.5,-0.866025403784439));
#13263=DIRECTION('center_axis',(0.,0.,1.));
#13264=DIRECTION('ref_axis',(1.,0.,0.));
#13265=DIRECTION('',(-1.,0.,0.));
#13266=DIRECTION('',(0.,1.,0.));
#13267=DIRECTION('',(0.,1.,0.));
#13268=DIRECTION('center_axis',(0.,-0.866025403784439,0.5));
#13269=DIRECTION('ref_axis',(-1.,0.,0.));
#13270=DIRECTION('',(-1.,0.,0.));
#13271=DIRECTION('',(0.,0.5,0.866025403784439));
#13272=DIRECTION('',(0.,0.5,0.866025403784439));
#13273=DIRECTION('center_axis',(0.,-0.866025403784439,-0.5));
#13274=DIRECTION('ref_axis',(0.,0.5,-0.866025403784439));
#13275=DIRECTION('',(-1.,0.,0.));
#13276=DIRECTION('',(0.,-0.5,0.866025403784439));
#13277=DIRECTION('',(0.,-0.5,0.866025403784439));
#13278=DIRECTION('center_axis',(0.,0.,-1.));
#13279=DIRECTION('ref_axis',(0.,-1.,0.));
#13280=DIRECTION('',(0.,-1.,0.));
#13281=DIRECTION('',(0.,-1.,0.));
#13282=DIRECTION('center_axis',(-1.,0.,0.));
#13283=DIRECTION('ref_axis',(0.,0.,1.));
#13284=DIRECTION('center_axis',(-1.,0.,0.));
#13285=DIRECTION('ref_axis',(0.,0.,1.));
#13286=DIRECTION('center_axis',(-1.,0.,0.));
#13287=DIRECTION('ref_axis',(0.,0.,1.));
#13288=DIRECTION('center_axis',(-1.,0.,0.));
#13289=DIRECTION('ref_axis',(0.,0.,1.));
#13290=DIRECTION('center_axis',(-1.,0.,0.));
#13291=DIRECTION('ref_axis',(0.,0.,1.));
#13292=DIRECTION('center_axis',(-1.,0.,0.));
#13293=DIRECTION('ref_axis',(0.,0.,1.));
#13294=DIRECTION('center_axis',(-1.,0.,0.));
#13295=DIRECTION('ref_axis',(0.,0.,1.));
#17441=CARTESIAN_POINT('',(0.,0.,0.));
#17442=CARTESIAN_POINT('Origin',(4.0132,0.,0.));
#17443=CARTESIAN_POINT('',(4.0132,-6.73445521319121E-16,5.4991));
#17444=CARTESIAN_POINT('Origin',(4.0132,0.,0.));
#17445=CARTESIAN_POINT('',(3.6068,0.,5.4991));
#17446=CARTESIAN_POINT('',(4.0132,-6.73445521319121E-16,5.4991));
#17447=CARTESIAN_POINT('',(3.6068,-4.76236029795101,2.74955));
#17448=CARTESIAN_POINT('Origin',(3.6068,0.,0.));
#17449=CARTESIAN_POINT('',(3.6068,-4.76236029795101,-2.74955));
#17450=CARTESIAN_POINT('Origin',(3.6068,0.,0.));
#17451=CARTESIAN_POINT('',(3.6068,0.,-5.4991));
#17452=CARTESIAN_POINT('Origin',(3.6068,0.,0.));
#17453=CARTESIAN_POINT('',(3.6068,4.76236029795101,-2.74955));
#17454=CARTESIAN_POINT('Origin',(3.6068,0.,0.));
#17455=CARTESIAN_POINT('',(3.6068,4.76236029795101,2.74955));
#17456=CARTESIAN_POINT('Origin',(3.6068,0.,0.));
#17457=CARTESIAN_POINT('Origin',(3.6068,0.,0.));
#17458=CARTESIAN_POINT('Origin',(0.,0.,0.));
#17459=CARTESIAN_POINT('',(0.68707,3.04683551100267E-16,2.48793));
#17460=CARTESIAN_POINT('',(0.687070000000001,-3.04683551100267E-16,-2.48793));
#17461=CARTESIAN_POINT('Origin',(0.68707,0.,0.));
#17462=CARTESIAN_POINT('',(-2.24879295770376E-16,-3.88825358729285E-16,
-3.175));
#17463=CARTESIAN_POINT('',(0.,-3.88825358729285E-16,-3.175));
#17464=CARTESIAN_POINT('Origin',(0.,0.,0.));
#17465=CARTESIAN_POINT('Origin',(0.68707,0.,0.));
#17466=CARTESIAN_POINT('Origin',(4.0132,0.,0.));
#17467=CARTESIAN_POINT('',(3.32613,-3.04683551100267E-16,2.48793));
#17468=CARTESIAN_POINT('',(4.0132,-3.04683551100267E-16,2.48793));
#17469=CARTESIAN_POINT('Origin',(3.32613,0.,0.));
#17470=CARTESIAN_POINT('Origin',(3.32613,0.,0.));
#17471=CARTESIAN_POINT('',(4.0132,-3.88825358729285E-16,3.175));
#17472=CARTESIAN_POINT('',(3.32613,-3.04683551100267E-16,2.48793));
#17473=CARTESIAN_POINT('Origin',(4.0132,0.,0.));
#17474=CARTESIAN_POINT('Origin',(0.,0.,0.));
#17475=CARTESIAN_POINT('',(-1.45255548274778E-16,-4.76236029795101,2.74955));
#17476=CARTESIAN_POINT('',(0.227948057104695,-3.17490686530067,5.4991));
#17477=CARTESIAN_POINT('Ctrl Pts',(-6.0638607167382E-16,-4.76236029795101,
2.74954999999999));
#17478=CARTESIAN_POINT('Ctrl Pts',(-9.99200722162641E-16,-4.02562059590196,
4.0256205959021));
#17479=CARTESIAN_POINT('Ctrl Pts',(0.227948057104729,-3.17490686530054,
5.49910000000022));
#17480=CARTESIAN_POINT('',(0.,0.,5.4991));
#17481=CARTESIAN_POINT('Ctrl Pts',(0.227948057104731,-3.17490686530094,
5.4991));
#17482=CARTESIAN_POINT('Ctrl Pts',(1.89523333747949E-16,-1.47347940409809,
5.4991));
#17483=CARTESIAN_POINT('Ctrl Pts',(3.46506326670755E-16,1.38602530668302E-15,
5.4991));
#17484=CARTESIAN_POINT('Origin',(0.,0.,0.));
#17485=CARTESIAN_POINT('Origin',(0.,0.,0.));
#17486=CARTESIAN_POINT('',(0.,0.,-5.4991));
#17487=CARTESIAN_POINT('',(-1.45255548274778E-16,4.76236029795101,-2.74955));
#17488=CARTESIAN_POINT('Origin',(0.,0.,0.));
#17489=CARTESIAN_POINT('',(-8.71533289648669E-17,-4.76236029795101,-2.74955));
#17490=CARTESIAN_POINT('Origin',(0.,0.,0.));
#17491=CARTESIAN_POINT('Origin',(0.,0.,0.));
#17492=CARTESIAN_POINT('',(-8.71533289648669E-17,4.76236029795101,2.74955));
#17493=CARTESIAN_POINT('Origin',(0.,0.,0.));
#17494=CARTESIAN_POINT('Origin',(0.,0.,0.));
#17495=CARTESIAN_POINT('Origin',(0.,0.,0.));
#17496=CARTESIAN_POINT('',(0.227948057104695,3.17490686530067,-5.4991));
#17497=CARTESIAN_POINT('Ctrl Pts',(-6.0638607167382E-16,4.76236029795101,
-2.74954999999999));
#17498=CARTESIAN_POINT('Ctrl Pts',(-9.99200722162641E-16,4.02562059590196,
-4.0256205959021));
#17499=CARTESIAN_POINT('Ctrl Pts',(0.227948057104729,3.17490686530054,-5.49910000000022));
#17500=CARTESIAN_POINT('Ctrl Pts',(0.227948057104731,3.17490686530094,-5.4991));
#17501=CARTESIAN_POINT('Ctrl Pts',(1.89523333747949E-16,1.47347940409809,
-5.4991));
#17502=CARTESIAN_POINT('Ctrl Pts',(3.46506326670755E-16,-1.38602530668302E-15,
-5.4991));
#17503=CARTESIAN_POINT('Origin',(0.,0.,0.));
#17504=CARTESIAN_POINT('',(0.227948057104695,-3.17490686530067,-5.4991));
#17505=CARTESIAN_POINT('Ctrl Pts',(3.46506326670755E-16,-1.38602530668302E-15,
-5.4991));
#17506=CARTESIAN_POINT('Ctrl Pts',(4.71844785465692E-16,-1.47347940409809,
-5.4991));
#17507=CARTESIAN_POINT('Ctrl Pts',(0.227948057104729,-3.17490686530093,
-5.4991));
#17508=CARTESIAN_POINT('Ctrl Pts',(0.22794805710473,-3.17490686530054,-5.49910000000023));
#17509=CARTESIAN_POINT('Ctrl Pts',(-4.36421435310789E-16,-4.02562059590196,
-4.02562059590211));
#17510=CARTESIAN_POINT('Ctrl Pts',(-6.06386071673821E-16,-4.762360297951,
-2.74955));
#17511=CARTESIAN_POINT('Origin',(0.,0.,0.));
#17512=CARTESIAN_POINT('',(0.227948057104694,-6.34981373060134,-4.28887208897701E-17));
#17513=CARTESIAN_POINT('Ctrl Pts',(-6.06386071673821E-16,-4.762360297951,
-2.74955));
#17514=CARTESIAN_POINT('Ctrl Pts',(-8.04911692853238E-16,-5.49910000000005,
-1.4734794040979));
#17515=CARTESIAN_POINT('Ctrl Pts',(0.227948057104729,-6.34981373060147,
2.26225062694678E-13));
#17516=CARTESIAN_POINT('Ctrl Pts',(0.227948057104729,-6.34981373060147,
-2.28464914800566E-13));
#17517=CARTESIAN_POINT('Ctrl Pts',(-9.3584922122824E-17,-5.49910000000005,
1.47347940409789));
#17518=CARTESIAN_POINT('Ctrl Pts',(-6.0638607167382E-16,-4.76236029795101,
2.74954999999999));
#17519=CARTESIAN_POINT('Origin',(0.,0.,0.));
#17520=CARTESIAN_POINT('',(0.227948057104695,3.17490686530067,5.4991));
#17521=CARTESIAN_POINT('Ctrl Pts',(3.46506326670755E-16,1.38602530668302E-15,
5.4991));
#17522=CARTESIAN_POINT('Ctrl Pts',(4.71844785465692E-16,1.47347940409809,
5.4991));
#17523=CARTESIAN_POINT('Ctrl Pts',(0.227948057104729,3.17490686530093,5.4991));
#17524=CARTESIAN_POINT('Ctrl Pts',(0.22794805710473,3.17490686530054,5.49910000000023));
#17525=CARTESIAN_POINT('Ctrl Pts',(-4.36421435310789E-16,4.02562059590196,
4.02562059590211));
#17526=CARTESIAN_POINT('Ctrl Pts',(-6.06386071673821E-16,4.762360297951,
2.74955));
#17527=CARTESIAN_POINT('Origin',(0.,0.,0.));
#17528=CARTESIAN_POINT('',(0.227948057104694,6.34981373060134,4.28887208897701E-17));
#17529=CARTESIAN_POINT('Ctrl Pts',(-6.06386071673821E-16,4.762360297951,
2.74955));
#17530=CARTESIAN_POINT('Ctrl Pts',(-8.04911692853238E-16,5.49910000000005,
1.4734794040979));
#17531=CARTESIAN_POINT('Ctrl Pts',(0.227948057104729,6.34981373060147,-2.26225062694678E-13));
#17532=CARTESIAN_POINT('Ctrl Pts',(0.227948057104729,6.34981373060147,2.28464914800566E-13));
#17533=CARTESIAN_POINT('Ctrl Pts',(-9.3584922122824E-17,5.49910000000005,
-1.47347940409789));
#17534=CARTESIAN_POINT('Ctrl Pts',(-6.0638607167382E-16,4.76236029795101,
-2.74954999999999));
#17535=CARTESIAN_POINT('Origin',(4.0132,-3.17490686530067,5.4991));
#17536=CARTESIAN_POINT('',(3.6068,-6.34981373060134,0.));
#17537=CARTESIAN_POINT('',(4.0132,-6.34981373060134,0.));
#17538=CARTESIAN_POINT('',(3.6068,-3.112630297951,5.60696617877061));
#17539=CARTESIAN_POINT('',(3.6068,-3.17490686530067,5.4991));
#17540=CARTESIAN_POINT('',(3.6068,-3.112630297951,5.60696617877061));
#17541=CARTESIAN_POINT('',(4.0132,-3.17490686530067,5.4991));
#17542=CARTESIAN_POINT('Origin',(4.0132,-6.34981373060134,0.));
#17543=CARTESIAN_POINT('',(3.6068,-3.17490686530067,-5.4991));
#17544=CARTESIAN_POINT('',(4.0132,-3.17490686530067,-5.4991));
#17545=CARTESIAN_POINT('',(3.6068,-3.112630297951,-5.60696617877061));
#17546=CARTESIAN_POINT('',(3.6068,-3.112630297951,-5.60696617877061));
#17547=CARTESIAN_POINT('Origin',(4.0132,-3.17490686530067,-5.4991));
#17548=CARTESIAN_POINT('',(3.6068,3.17490686530067,-5.4991));
#17549=CARTESIAN_POINT('',(4.0132,3.17490686530067,-5.4991));
#17550=CARTESIAN_POINT('',(3.6068,6.59892,-5.4991));
#17551=CARTESIAN_POINT('',(3.6068,6.59892,-5.4991));
#17552=CARTESIAN_POINT('Origin',(4.0132,3.17490686530067,-5.4991));
#17553=CARTESIAN_POINT('',(3.6068,6.34981373060134,0.));
#17554=CARTESIAN_POINT('',(4.0132,6.34981373060134,0.));
#17555=CARTESIAN_POINT('',(3.6068,6.41209029795101,0.107866178770604));
#17556=CARTESIAN_POINT('',(3.6068,6.41209029795101,0.107866178770604));
#17557=CARTESIAN_POINT('Origin',(4.0132,6.34981373060134,0.));
#17558=CARTESIAN_POINT('',(3.6068,3.17490686530067,5.4991));
#17559=CARTESIAN_POINT('',(4.0132,3.17490686530067,5.4991));
#17560=CARTESIAN_POINT('',(3.6068,6.41209029795101,-0.107866178770604));
#17561=CARTESIAN_POINT('',(3.6068,6.41209029795101,-0.107866178770604));
#17562=CARTESIAN_POINT('Origin',(4.0132,3.17490686530067,5.4991));
#17563=CARTESIAN_POINT('',(3.6068,6.59892,5.4991));
#17564=CARTESIAN_POINT('',(3.6068,6.59892,5.4991));
#17565=CARTESIAN_POINT('Origin',(4.0132,5.4991,0.));
#17566=CARTESIAN_POINT('Origin',(3.6068,6.59892,0.));
#17567=CARTESIAN_POINT('Origin',(3.6068,6.59892,0.));
#17568=CARTESIAN_POINT('Origin',(3.6068,6.59892,0.));
#17569=CARTESIAN_POINT('Origin',(3.6068,6.59892,0.));
#17570=CARTESIAN_POINT('Origin',(3.6068,6.59892,0.));
#17571=CARTESIAN_POINT('Origin',(3.6068,6.59892,0.));
#17979=UNCERTAINTY_MEASURE_WITH_UNIT(LENGTH_MEASURE(0.01),#18007,
'DISTANCE_ACCURACY_VALUE',
'Maximum model space distance between geometric entities at asserted c
onnectivities');
#17986=UNCERTAINTY_MEASURE_WITH_UNIT(LENGTH_MEASURE(0.01),#18007,
'DISTANCE_ACCURACY_VALUE',
'Maximum model space distance between geometric entities at asserted c
onnectivities');
#17999=(
GEOMETRIC_REPRESENTATION_CONTEXT(3)
GLOBAL_UNCERTAINTY_ASSIGNED_CONTEXT((#17979))
GLOBAL_UNIT_ASSIGNED_CONTEXT((#18007,#18009,#18010))
REPRESENTATION_CONTEXT('','3D')
);
#18006=(
GEOMETRIC_REPRESENTATION_CONTEXT(3)
GLOBAL_UNCERTAINTY_ASSIGNED_CONTEXT((#17986))
GLOBAL_UNIT_ASSIGNED_CONTEXT((#18007,#18009,#18010))
REPRESENTATION_CONTEXT('','3D')
);
#18007=(
LENGTH_UNIT()
NAMED_UNIT(*)
SI_UNIT(.MILLI.,.METRE.)
);
#18009=(
NAMED_UNIT(*)
PLANE_ANGLE_UNIT()
SI_UNIT($,.RADIAN.)
);
#18010=(
NAMED_UNIT(*)
SI_UNIT($,.STERADIAN.)
SOLID_ANGLE_UNIT()
);
#18023=SHAPE_DEFINITION_REPRESENTATION(#18042,#18082);
#18042=PRODUCT_DEFINITION_SHAPE('',$,#18102);
#18082=SHAPE_REPRESENTATION('',(#10592),#17999);
#18089=PRODUCT_DEFINITION_CONTEXT('part definition',#18148,'design');
#18102=PRODUCT_DEFINITION('Axle Nut','Axle Nut',#18121,#18089);
#18121=PRODUCT_DEFINITION_FORMATION('',$,#18162);
#18148=APPLICATION_CONTEXT(
'Core Data for Automotive Mechanical Design Process');
#18149=PRODUCT_CONTEXT('part definition',#18148,'mechanical');
#18162=PRODUCT('Axle Nut','Axle Nut',$,(#18149));
#18172=PRESENTATION_STYLE_ASSIGNMENT((#18176));
#18176=SURFACE_STYLE_USAGE(.BOTH.,#18180);
#18180=SURFACE_SIDE_STYLE('',(#18184));
#18184=SURFACE_STYLE_FILL_AREA(#18188);
#18188=FILL_AREA_STYLE('Opaque(97,158,199)',(#18192));
#18192=FILL_AREA_STYLE_COLOUR('Opaque(97,158,199)',#18196);
#18196=COLOUR_RGB('Opaque(97,158,199)',0.380392156862745,0.619607843137255,
0.780392156862745);
ENDSEC;
END-ISO-10303-21;
